ISO-10303-21;
HEADER;
FILE_DESCRIPTION((''),'2;1');
FILE_NAME('Shaft Spacer Washer D22.4.step','2026-10-06T07:01:46+05:00',(''),(''),'','','');
FILE_SCHEMA (('AUTOMOTIVE_DESIGN { 1 0 10303 214 3 1 1 }'));
ENDSEC;
DATA;
#10=MECHANICAL_DESIGN_GEOMETRIC_PRESENTATION_REPRESENTATION('',(#149),#11396);
#119=SHAPE_REPRESENTATION_RELATIONSHIP('SRR','None',#11466,#134) ;
#134=ADVANCED_BREP_SHAPE_REPRESENTATION('',(#164),#11392) ;
#149=STYLED_ITEM('',(#11550),#164) ;
#164=MANIFOLD_SOLID_BREP('Shaft Spacer Washer D22.4',#5580) ;
#372=FACE_BOUND('',#1186,.T.) ;
#373=FACE_BOUND('',#1189,.T.) ;
#492=PLANE('',#6333) ;
#493=PLANE('',#6337) ;
#813=FACE_OUTER_BOUND('',#1184,.T.) ;
#814=FACE_OUTER_BOUND('',#1185,.T.) ;
#815=FACE_OUTER_BOUND('',#1187,.T.) ;
#816=FACE_OUTER_BOUND('',#1188,.T.) ;
#1184=EDGE_LOOP('',(#4954,#4955,#4956,#4957)) ;
#1185=EDGE_LOOP('',(#4958)) ;
#1186=EDGE_LOOP('',(#4959)) ;
#1187=EDGE_LOOP('',(#4960,#4961,#4962,#4963)) ;
#1188=EDGE_LOOP('',(#4964)) ;
#1189=EDGE_LOOP('',(#4965)) ;
#1565=LINE('',#11197,#1948) ;
#1566=LINE('',#11205,#1949) ;
#1948=VECTOR('',#7923,3.985) ;
#1949=VECTOR('',#7934,5.595) ;
#2239=CIRCLE('',#6331,3.985) ;
#2240=CIRCLE('',#6332,3.985) ;
#2241=CIRCLE('',#6334,5.595) ;
#2242=CIRCLE('',#6336,5.595) ;
#2700=VERTEX_POINT('',#11194) ;
#2701=VERTEX_POINT('',#11196) ;
#2702=VERTEX_POINT('',#11200) ;
#2703=VERTEX_POINT('',#11203) ;
#3459=EDGE_CURVE('',#2700,#2700,#2239,.T.) ;
#3460=EDGE_CURVE('',#2700,#2701,#1565,.T.) ;
#3461=EDGE_CURVE('',#2701,#2701,#2240,.T.) ;
#3462=EDGE_CURVE('',#2702,#2702,#2241,.T.) ;
#3463=EDGE_CURVE('',#2703,#2703,#2242,.T.) ;
#3464=EDGE_CURVE('',#2703,#2702,#1566,.T.) ;
#4954=ORIENTED_EDGE('',*,*,#3459,.T.) ;
#4955=ORIENTED_EDGE('',*,*,#3460,.T.) ;
#4956=ORIENTED_EDGE('',*,*,#3461,.F.) ;
#4957=ORIENTED_EDGE('',*,*,#3460,.F.) ;
#4958=ORIENTED_EDGE('',*,*,#3462,.F.) ;
#4959=ORIENTED_EDGE('',*,*,#3461,.T.) ;
#4960=ORIENTED_EDGE('',*,*,#3463,.F.) ;
#4961=ORIENTED_EDGE('',*,*,#3464,.T.) ;
#4962=ORIENTED_EDGE('',*,*,#3462,.T.) ;
#4963=ORIENTED_EDGE('',*,*,#3464,.F.) ;
#4964=ORIENTED_EDGE('',*,*,#3463,.T.) ;
#4965=ORIENTED_EDGE('',*,*,#3459,.F.) ;
#5218=CYLINDRICAL_SURFACE('',#6330,3.985) ;
#5219=CYLINDRICAL_SURFACE('',#6335,5.595) ;
#5538=ADVANCED_FACE('',(#813),#5218,.F.) ;
#5539=ADVANCED_FACE('',(#814,#372),#492,.T.) ;
#5540=ADVANCED_FACE('',(#815),#5219,.T.) ;
#5541=ADVANCED_FACE('',(#816,#373),#493,.T.) ;
#5580=CLOSED_SHELL('',(#5538,#5539,#5540,#5541)) ;
#6329=AXIS2_PLACEMENT_3D('',#11192,#7917,#7918) ;
#6330=AXIS2_PLACEMENT_3D('',#11193,#7919,#7920) ;
#6331=AXIS2_PLACEMENT_3D('',#11195,#7921,#7922) ;
#6332=AXIS2_PLACEMENT_3D('',#11198,#7924,#7925) ;
#6333=AXIS2_PLACEMENT_3D('',#11199,#7926,#7927) ;
#6334=AXIS2_PLACEMENT_3D('',#11201,#7928,#7929) ;
#6335=AXIS2_PLACEMENT_3D('',#11202,#7930,#7931) ;
#6336=AXIS2_PLACEMENT_3D('',#11204,#7932,#7933) ;
#6337=AXIS2_PLACEMENT_3D('',#11206,#7935,#7936) ;
#7917=DIRECTION('axis',(0.,0.,1.)) ;
#7918=DIRECTION('refdir',(1.,0.,0.)) ;
#7919=DIRECTION('center_axis',(1.,0.,0.)) ;
#7920=DIRECTION('ref_axis',(0.,1.,0.)) ;
#7921=DIRECTION('center_axis',(1.,0.,0.)) ;
#7922=DIRECTION('ref_axis',(0.,0.,-1.)) ;
#7923=DIRECTION('',(-1.,0.,0.)) ;
#7924=DIRECTION('center_axis',(1.,0.,0.)) ;
#7925=DIRECTION('ref_axis',(0.,0.,-1.)) ;
#7926=DIRECTION('center_axis',(-1.,0.,0.)) ;
#7927=DIRECTION('ref_axis',(0.,0.,1.)) ;
#7928=DIRECTION('center_axis',(1.,0.,0.)) ;
#7929=DIRECTION('ref_axis',(0.,0.,-1.)) ;
#7930=DIRECTION('center_axis',(1.,0.,0.)) ;
#7931=DIRECTION('ref_axis',(0.,1.,0.)) ;
#7932=DIRECTION('center_axis',(1.,0.,0.)) ;
#7933=DIRECTION('ref_axis',(0.,0.,-1.)) ;
#7934=DIRECTION('',(-1.,0.,0.)) ;
#7935=DIRECTION('center_axis',(1.,0.,0.)) ;
#7936=DIRECTION('ref_axis',(0.,0.,-1.)) ;
#11192=CARTESIAN_POINT('',(0.,0.,0.)) ;
#11193=CARTESIAN_POINT('Origin',(-15.565,17.565,27.14)) ;
#11194=CARTESIAN_POINT('',(-15.34,13.58,27.14)) ;
#11195=CARTESIAN_POINT('Origin',(-15.34,17.565,27.14)) ;
#11196=CARTESIAN_POINT('',(-15.79,13.58,27.14)) ;
#11197=CARTESIAN_POINT('',(-15.565,13.58,27.14)) ;
#11198=CARTESIAN_POINT('Origin',(-15.79,17.565,27.14)) ;
#11199=CARTESIAN_POINT('Origin',(-15.79,23.16,27.14)) ;
#11200=CARTESIAN_POINT('',(-15.79,11.97,27.14)) ;
#11201=CARTESIAN_POINT('Origin',(-15.79,17.565,27.14)) ;
#11202=CARTESIAN_POINT('Origin',(-15.565,17.565,27.14)) ;
#11203=CARTESIAN_POINT('',(-15.34,11.97,27.14)) ;
#11204=CARTESIAN_POINT('Origin',(-15.34,17.565,27.14)) ;
#11205=CARTESIAN_POINT('',(-15.565,11.97,27.14)) ;
#11206=CARTESIAN_POINT('Origin',(-15.34,21.55,27.14)) ;
#11375=UNCERTAINTY_MEASURE_WITH_UNIT(LENGTH_MEASURE(0.01),#11397,
'DISTANCE_ACCURACY_VALUE',
'Maximum model space distance between geometric entities at asserted c
onnectivities') ;
#11379=UNCERTAINTY_MEASURE_WITH_UNIT(LENGTH_MEASURE(0.01),#11397,
'DISTANCE_ACCURACY_VALUE',
'Maximum model space distance between geometric entities at asserted c
onnectivities') ;
#11392=(
GEOMETRIC_REPRESENTATION_CONTEXT(3)
GLOBAL_UNCERTAINTY_ASSIGNED_CONTEXT((#11375))
GLOBAL_UNIT_ASSIGNED_CONTEXT((#11397,#11399,#11400))
REPRESENTATION_CONTEXT('','3D')
) ;
#11396=(
GEOMETRIC_REPRESENTATION_CONTEXT(3)
GLOBAL_UNCERTAINTY_ASSIGNED_CONTEXT((#11379))
GLOBAL_UNIT_ASSIGNED_CONTEXT((#11397,#11399,#11400))
REPRESENTATION_CONTEXT('','3D')
) ;
#11397=(
LENGTH_UNIT()
NAMED_UNIT(*)
SI_UNIT(.MILLI.,.METRE.)
) ;
#11399=(
NAMED_UNIT(*)
PLANE_ANGLE_UNIT()
SI_UNIT($,.RADIAN.)
) ;
#11400=(
NAMED_UNIT(*)
SI_UNIT($,.STERADIAN.)
SOLID_ANGLE_UNIT()
) ;
#11413=SHAPE_DEFINITION_REPRESENTATION(#11429,#11466) ;
#11429=PRODUCT_DEFINITION_SHAPE('',$,#11483) ;
#11466=SHAPE_REPRESENTATION('',(#6329),#11392) ;
#11470=PRODUCT_DEFINITION_CONTEXT('part definition',#11520,'design') ;
#11483=PRODUCT_DEFINITION('Shaft Spacer Washer D22.4',
'Shaft Spacer Washer D22.4',#11499,#11470) ;
#11499=PRODUCT_DEFINITION_FORMATION('',$,#11534) ;
#11520=APPLICATION_CONTEXT(
'Core Data for Automotive Mechanical Design Process') ;
#11521=PRODUCT_CONTEXT('part definition',#11520,'mechanical') ;
#11534=PRODUCT('Shaft Spacer Washer D22.4','Shaft Spacer Washer D22.4',$,
(#11521)) ;
#11550=PRESENTATION_STYLE_ASSIGNMENT((#11566)) ;
#11566=SURFACE_STYLE_USAGE(.BOTH.,#11582) ;
#11582=SURFACE_SIDE_STYLE('',(#11598)) ;
#11598=SURFACE_STYLE_FILL_AREA(#11614) ;
#11614=FILL_AREA_STYLE('MAS-252 Metallic - Shaft Spacer Washer D22.4',(#11630)) ;
#11630=FILL_AREA_STYLE_COLOUR(
'MAS-252 Metallic - Shaft Spacer Washer D22.4',#11646) ;
#11646=COLOUR_RGB('MAS-252 Metallic - Shaft Spacer Washer D22.4', 0.08235294, 0.09019608, 0.10196078) ;
ENDSEC;
END-ISO-10303-21;
